ISO-10303-21;
HEADER;
/* Generated by software containing ST-Developer
 * from STEP Tools, Inc. (www.steptools.com) 
 */
/* OPTION: using custom renumber hook */

FILE_DESCRIPTION(
/* description */ ('STEP AP242 Edition 2', 'CAx-IF Rec.Pracs.---Representation and Presentation of Product Manufa
cturing Information (PMI)---4.0---2014-10-13', 'CAx-IF Rec.Pracs.---3D Tessellated Geometry---0.4---2014-09-14', '2;1', 'CAx-IF Rec.Pracs.---User Defined Attributes---1.5---2016-08-15'),
/* implementation_level */ '2;1');

FILE_NAME(
/* name */ 'endcap__ DE    14671.step',
/* time_stamp */ '2026-10-09T00:23:50Z',
/* author */ (''),
/* organization */ (''),
/* preprocessor_version */ 'ST-DEVELOPER v20',
/* originating_system */ 'ONSHAPE BY PTC INC, 1.221',
/* authorisation */ '  ');

FILE_SCHEMA (('AP242_MANAGED_MODEL_BASED_3D_ENGINEERING_MIM_LF { 1 0 10303 442 3 1 4 }'));
ENDSEC;

DATA;
#24=CONICAL_SURFACE('',#8604,0.,0.78539816339745);
#44=TOROIDAL_SURFACE('',#8585,0.00799999999990077,0.000500000000345792);
#45=TOROIDAL_SURFACE('',#8587,0.0109999999999008,0.00050000000034579);
#46=TOROIDAL_SURFACE('',#8591,0.00799999999990077,0.00050000000034579);
#47=TOROIDAL_SURFACE('',#8597,0.00950000000009923,0.000500000000345799);
#48=TOROIDAL_SURFACE('',#8599,0.00849999999905548,0.000499999999472932);
#49=TOROIDAL_SURFACE('',#8600,0.00849999999905548,0.000499999999472929);
#50=TOROIDAL_SURFACE('',#8606,0.00799999999935485,0.00100000000059717);
#51=TOROIDAL_SURFACE('',#8608,0.00799999999935485,0.00100000000059717);
#52=TOROIDAL_SURFACE('',#8609,0.00800000000094452,0.000499999999472942);
#53=TOROIDAL_SURFACE('',#8610,0.00800000000094452,0.000499999999472943);
#145=SHAPE_REPRESENTATION_RELATIONSHIP('','',#8235,#151);
#151=ADVANCED_BREP_SHAPE_REPRESENTATION('',(#8221),#18813);
#491=B_SPLINE_CURVE_WITH_KNOTS('',3,(#13170,#13171,#13172,#13173,#13174,
#13175,#13176,#13177,#13178,#13179,#13180),.UNSPECIFIED.,.F.,.F.,(4,1,1,
1,1,1,1,1,4),(1.82133646569706E-10,0.125000000151206,0.250000000120279,
0.375000000089351,0.500000000058424,0.625000000027496,0.749999999996569,
0.874999999965641,0.999999999934714),.UNSPECIFIED.);
#492=B_SPLINE_CURVE_WITH_KNOTS('',3,(#13185,#13186,#13187,#13188,#13189,
#13190,#13191,#13192,#13193,#13194,#13195),.UNSPECIFIED.,.F.,.F.,(4,1,1,
1,1,1,1,1,4),(0.,0.125,0.25,0.375,0.5,0.625,0.75,0.875,1.),
 .UNSPECIFIED.);
#493=B_SPLINE_CURVE_WITH_KNOTS('',3,(#13200,#13201,#13202,#13203,#13204,
#13205,#13206),.UNSPECIFIED.,.F.,.F.,(4,1,1,1,4),(1.08159974291989E-10,
0.250000000064798,0.500000000021436,0.749999999978074,0.999999999934712),
 .UNSPECIFIED.);
#494=B_SPLINE_CURVE_WITH_KNOTS('',3,(#13214,#13215,#13216,#13217,#13218,
#13219,#13220),.UNSPECIFIED.,.F.,.F.,(4,1,1,1,4),(0.,0.25,0.5,0.75,1.),
 .UNSPECIFIED.);
#495=B_SPLINE_CURVE_WITH_KNOTS('',3,(#13228,#13229,#13230,#13231,#13232,
#13233,#13234,#13235,#13236,#13237,#13238),.UNSPECIFIED.,.F.,.F.,(4,1,1,
1,1,1,1,1,4),(4.32086807808983E-11,0.125000000029647,0.250000000016085,
0.375000000002522,0.49999999998896,0.624999999975398,0.749999999961836,
0.874999999948274,0.999999999934712),.UNSPECIFIED.);
#496=B_SPLINE_CURVE_WITH_KNOTS('',3,(#13240,#13241,#13242,#13243),
 .UNSPECIFIED.,.F.,.F.,(4,4),(0.,1.),.UNSPECIFIED.);
#497=B_SPLINE_CURVE_WITH_KNOTS('',3,(#13245,#13246,#13247,#13248,#13249,
#13250,#13251),.UNSPECIFIED.,.F.,.F.,(4,1,1,1,4),(6.52880993013389E-11,
0.250000000020525,0.499999999975762,0.749999999930999,0.999999999886236),
 .UNSPECIFIED.);
#498=B_SPLINE_CURVE_WITH_KNOTS('',3,(#13253,#13254,#13255,#13256),
 .UNSPECIFIED.,.F.,.F.,(4,4),(0.,1.),.UNSPECIFIED.);
#499=B_SPLINE_CURVE_WITH_KNOTS('',3,(#13260,#13261,#13262,#13263,#13264,
#13265,#13266,#13267,#13268,#13269,#13270),.UNSPECIFIED.,.F.,.F.,(4,1,1,
1,1,1,1,1,4),(0.,0.125,0.25,0.375,0.5,0.625,0.75,0.875,1.),
 .UNSPECIFIED.);
#500=B_SPLINE_CURVE_WITH_KNOTS('',3,(#13278,#13279,#13280,#13281,#13282,
#13283,#13284,#13285,#13286,#13287,#13288),.UNSPECIFIED.,.F.,.F.,(4,1,1,
1,1,1,1,1,4),(0.,0.125,0.25,0.375,0.5,0.625,0.75,0.875,1.),
 .UNSPECIFIED.);
#501=B_SPLINE_CURVE_WITH_KNOTS('',3,(#13290,#13291,#13292,#13293),
 .UNSPECIFIED.,.F.,.F.,(4,4),(0.,1.),.UNSPECIFIED.);
#502=B_SPLINE_CURVE_WITH_KNOTS('',3,(#13297,#13298,#13299,#13300),
 .UNSPECIFIED.,.F.,.F.,(4,4),(0.,1.),.UNSPECIFIED.);
#503=B_SPLINE_CURVE_WITH_KNOTS('',3,(#13302,#13303,#13304,#13305,#13306,
#13307,#13308,#13309,#13310,#13311,#13312),.UNSPECIFIED.,.F.,.F.,(4,1,1,
1,1,1,1,1,4),(6.52871450848788E-11,0.125000000057126,0.250000000048965,
0.375000000040805,0.500000000032644,0.625000000024483,0.750000000016322,
0.875000000008161,1.),.UNSPECIFIED.);
#504=B_SPLINE_CURVE_WITH_KNOTS('',3,(#13314,#13315,#13316,#13317),
 .UNSPECIFIED.,.F.,.F.,(4,4),(0.,1.),.UNSPECIFIED.);
#505=B_SPLINE_CURVE_WITH_KNOTS('',3,(#13319,#13320,#13321,#13322,#13323,
#13324,#13325,#13326,#13327,#13328,#13329),.UNSPECIFIED.,.F.,.F.,(4,1,1,
1,1,1,1,1,4),(7.9578112254039E-11,0.12500000006147,0.250000000043362,0.375000000025254,
0.500000000007146,0.624999999989038,0.74999999997093,0.874999999952822,
0.999999999934714),.UNSPECIFIED.);
#506=B_SPLINE_CURVE_WITH_KNOTS('',3,(#13331,#13332,#13333,#13334),
 .UNSPECIFIED.,.F.,.F.,(4,4),(0.,1.),.UNSPECIFIED.);
#1036=PLANE('',#8581);
#1037=PLANE('',#8583);
#1038=PLANE('',#8593);
#2058=ORIENTED_EDGE('',*,*,#3950,.F.);
#2059=ORIENTED_EDGE('',*,*,#3951,.F.);
#2060=ORIENTED_EDGE('',*,*,#3952,.F.);
#2061=ORIENTED_EDGE('',*,*,#3950,.T.);
#2062=ORIENTED_EDGE('',*,*,#3953,.F.);
#2063=ORIENTED_EDGE('',*,*,#3951,.T.);
#2064=ORIENTED_EDGE('',*,*,#3954,.T.);
#2065=ORIENTED_EDGE('',*,*,#3955,.T.);
#2066=ORIENTED_EDGE('',*,*,#3952,.T.);
#2067=ORIENTED_EDGE('',*,*,#3953,.T.);
#2068=ORIENTED_EDGE('',*,*,#3956,.T.);
#2069=ORIENTED_EDGE('',*,*,#3954,.F.);
#2070=ORIENTED_EDGE('',*,*,#3955,.F.);
#2071=ORIENTED_EDGE('',*,*,#3957,.T.);
#2072=ORIENTED_EDGE('',*,*,#3958,.T.);
#2073=ORIENTED_EDGE('',*,*,#3958,.F.);
#2074=ORIENTED_EDGE('',*,*,#3957,.F.);
#2075=ORIENTED_EDGE('',*,*,#3959,.T.);
#2076=ORIENTED_EDGE('',*,*,#3960,.T.);
#2077=ORIENTED_EDGE('',*,*,#3956,.F.);
#2078=ORIENTED_EDGE('',*,*,#3961,.F.);
#2079=ORIENTED_EDGE('',*,*,#3960,.F.);
#2080=ORIENTED_EDGE('',*,*,#3959,.F.);
#2081=ORIENTED_EDGE('',*,*,#3962,.T.);
#2082=ORIENTED_EDGE('',*,*,#3963,.T.);
#2083=ORIENTED_EDGE('',*,*,#3964,.F.);
#2084=ORIENTED_EDGE('',*,*,#3965,.F.);
#2085=ORIENTED_EDGE('',*,*,#3961,.T.);
#2086=ORIENTED_EDGE('',*,*,#3966,.F.);
#2087=ORIENTED_EDGE('',*,*,#3967,.F.);
#2088=ORIENTED_EDGE('',*,*,#3968,.F.);
#2089=ORIENTED_EDGE('',*,*,#3962,.F.);
#2090=ORIENTED_EDGE('',*,*,#3963,.F.);
#2091=ORIENTED_EDGE('',*,*,#3968,.T.);
#2092=ORIENTED_EDGE('',*,*,#3969,.F.);
#2093=ORIENTED_EDGE('',*,*,#3966,.T.);
#2094=ORIENTED_EDGE('',*,*,#3970,.T.);
#2095=ORIENTED_EDGE('',*,*,#3971,.T.);
#2096=ORIENTED_EDGE('',*,*,#3964,.T.);
#2097=ORIENTED_EDGE('',*,*,#3965,.T.);
#2098=ORIENTED_EDGE('',*,*,#3972,.T.);
#2099=ORIENTED_EDGE('',*,*,#3973,.T.);
#2100=ORIENTED_EDGE('',*,*,#3967,.T.);
#2101=ORIENTED_EDGE('',*,*,#3969,.T.);
#2102=ORIENTED_EDGE('',*,*,#3971,.F.);
#2103=ORIENTED_EDGE('',*,*,#3974,.T.);
#2104=ORIENTED_EDGE('',*,*,#3975,.T.);
#2105=ORIENTED_EDGE('',*,*,#3976,.T.);
#2106=ORIENTED_EDGE('',*,*,#3974,.F.);
#2107=ORIENTED_EDGE('',*,*,#3970,.F.);
#2108=ORIENTED_EDGE('',*,*,#3976,.F.);
#2109=ORIENTED_EDGE('',*,*,#3977,.T.);
#2110=ORIENTED_EDGE('',*,*,#3978,.T.);
#2111=ORIENTED_EDGE('',*,*,#3979,.T.);
#2112=ORIENTED_EDGE('',*,*,#3980,.T.);
#2113=ORIENTED_EDGE('',*,*,#3973,.F.);
#2114=ORIENTED_EDGE('',*,*,#3981,.T.);
#2115=ORIENTED_EDGE('',*,*,#3978,.F.);
#2116=ORIENTED_EDGE('',*,*,#3972,.F.);
#2117=ORIENTED_EDGE('',*,*,#3980,.F.);
#2118=ORIENTED_EDGE('',*,*,#3979,.F.);
#2119=ORIENTED_EDGE('',*,*,#3981,.F.);
#2120=ORIENTED_EDGE('',*,*,#3975,.F.);
#2121=ORIENTED_EDGE('',*,*,#3977,.F.);
#3950=EDGE_CURVE('',#4971,#4971,#5645,.F.);
#3951=EDGE_CURVE('',#4972,#4972,#5646,.T.);
#3952=EDGE_CURVE('',#4973,#4973,#5647,.F.);
#3953=EDGE_CURVE('',#4974,#4974,#5648,.T.);
#3954=EDGE_CURVE('',#4975,#4976,#5649,.T.);
#3955=EDGE_CURVE('',#4976,#4975,#491,.T.);
#3956=EDGE_CURVE('',#4977,#4977,#5650,.F.);
#3957=EDGE_CURVE('',#4978,#4979,#492,.F.);
#3958=EDGE_CURVE('',#4979,#4978,#5651,.F.);
#3959=EDGE_CURVE('',#4980,#4981,#493,.T.);
#3960=EDGE_CURVE('',#4981,#4980,#5652,.T.);
#3961=EDGE_CURVE('',#4982,#4982,#5653,.T.);
#3962=EDGE_CURVE('',#4983,#4984,#494,.F.);
#3963=EDGE_CURVE('',#4984,#4983,#5654,.F.);
#3964=EDGE_CURVE('',#4985,#4986,#5655,.F.);
#3965=EDGE_CURVE('',#4986,#4985,#495,.T.);
#3966=EDGE_CURVE('',#4987,#4983,#496,.T.);
#3967=EDGE_CURVE('',#4988,#4987,#497,.T.);
#3968=EDGE_CURVE('',#4984,#4988,#498,.T.);
#3969=EDGE_CURVE('',#4987,#4988,#5656,.T.);
#3970=EDGE_CURVE('',#4989,#4990,#499,.F.);
#3971=EDGE_CURVE('',#4990,#4989,#5657,.T.);
#3972=EDGE_CURVE('',#4991,#4992,#5658,.F.);
#3973=EDGE_CURVE('',#4992,#4991,#500,.F.);
#3974=EDGE_CURVE('',#4990,#4993,#501,.T.);
#3975=EDGE_CURVE('',#4993,#4994,#5659,.F.);
#3976=EDGE_CURVE('',#4994,#4989,#502,.T.);
#3977=EDGE_CURVE('',#4994,#4993,#503,.T.);
#3978=EDGE_CURVE('',#4992,#4995,#504,.T.);
#3979=EDGE_CURVE('',#4995,#4996,#505,.T.);
#3980=EDGE_CURVE('',#4996,#4991,#506,.T.);
#3981=EDGE_CURVE('',#4996,#4995,#5660,.T.);
#4971=VERTEX_POINT('',#13157);
#4972=VERTEX_POINT('',#13159);
#4973=VERTEX_POINT('',#13162);
#4974=VERTEX_POINT('',#13165);
#4975=VERTEX_POINT('',#13168);
#4976=VERTEX_POINT('',#13169);
#4977=VERTEX_POINT('',#13183);
#4978=VERTEX_POINT('',#13196);
#4979=VERTEX_POINT('',#13197);
#4980=VERTEX_POINT('',#13207);
#4981=VERTEX_POINT('',#13208);
#4982=VERTEX_POINT('',#13212);
#4983=VERTEX_POINT('',#13221);
#4984=VERTEX_POINT('',#13222);
#4985=VERTEX_POINT('',#13226);
#4986=VERTEX_POINT('',#13227);
#4987=VERTEX_POINT('',#13244);
#4988=VERTEX_POINT('',#13252);
#4989=VERTEX_POINT('',#13271);
#4990=VERTEX_POINT('',#13272);
#4991=VERTEX_POINT('',#13276);
#4992=VERTEX_POINT('',#13277);
#4993=VERTEX_POINT('',#13294);
#4994=VERTEX_POINT('',#13296);
#4995=VERTEX_POINT('',#13318);
#4996=VERTEX_POINT('',#13330);
#5645=CIRCLE('',#8579,0.0075);
#5646=CIRCLE('',#8580,0.0075);
#5647=CIRCLE('',#8582,0.00800000000055703);
#5648=CIRCLE('',#8584,0.011000000000557);
#5649=CIRCLE('',#8586,0.00850000000024656);
#5650=CIRCLE('',#8588,0.011000000000557);
#5651=CIRCLE('',#8590,0.0085);
#5652=CIRCLE('',#8592,0.00800000000055703);
#5653=CIRCLE('',#8594,0.00949999999944297);
#5654=CIRCLE('',#8596,0.008);
#5655=CIRCLE('',#8598,0.009);
#5656=CIRCLE('',#8601,0.00814644660912898);
#5657=CIRCLE('',#8603,0.009);
#5658=CIRCLE('',#8605,0.00835355339112897);
#5659=CIRCLE('',#8607,0.0085000000001643);
#5660=CIRCLE('',#8611,0.00850000000041746);
#6167=EDGE_LOOP('',(#2058));
#6168=EDGE_LOOP('',(#2059));
#6169=EDGE_LOOP('',(#2060));
#6170=EDGE_LOOP('',(#2061));
#6171=EDGE_LOOP('',(#2062));
#6172=EDGE_LOOP('',(#2063));
#6173=EDGE_LOOP('',(#2064,#2065));
#6174=EDGE_LOOP('',(#2066));
#6175=EDGE_LOOP('',(#2067));
#6176=EDGE_LOOP('',(#2068));
#6177=EDGE_LOOP('',(#2069,#2070));
#6178=EDGE_LOOP('',(#2071,#2072));
#6179=EDGE_LOOP('',(#2073,#2074));
#6180=EDGE_LOOP('',(#2075,#2076));
#6181=EDGE_LOOP('',(#2077));
#6182=EDGE_LOOP('',(#2078));
#6183=EDGE_LOOP('',(#2079,#2080));
#6184=EDGE_LOOP('',(#2081,#2082));
#6185=EDGE_LOOP('',(#2083,#2084));
#6186=EDGE_LOOP('',(#2085));
#6187=EDGE_LOOP('',(#2086,#2087,#2088,#2089));
#6188=EDGE_LOOP('',(#2090,#2091,#2092,#2093));
#6189=EDGE_LOOP('',(#2094,#2095));
#6190=EDGE_LOOP('',(#2096,#2097));
#6191=EDGE_LOOP('',(#2098,#2099));
#6192=EDGE_LOOP('',(#2100,#2101));
#6193=EDGE_LOOP('',(#2102,#2103,#2104,#2105));
#6194=EDGE_LOOP('',(#2106,#2107,#2108,#2109));
#6195=EDGE_LOOP('',(#2110,#2111,#2112,#2113));
#6196=EDGE_LOOP('',(#2114,#2115,#2116,#2117));
#6197=EDGE_LOOP('',(#2118,#2119));
#6198=EDGE_LOOP('',(#2120,#2121));
#6928=FACE_BOUND('',#6167,.T.);
#6929=FACE_BOUND('',#6168,.T.);
#6930=FACE_BOUND('',#6169,.T.);
#6931=FACE_BOUND('',#6170,.T.);
#6932=FACE_BOUND('',#6171,.T.);
#6933=FACE_BOUND('',#6172,.T.);
#6934=FACE_BOUND('',#6173,.T.);
#6935=FACE_BOUND('',#6174,.T.);
#6936=FACE_BOUND('',#6175,.T.);
#6937=FACE_BOUND('',#6176,.T.);
#6938=FACE_BOUND('',#6177,.T.);
#6939=FACE_BOUND('',#6178,.T.);
#6940=FACE_BOUND('',#6179,.T.);
#6941=FACE_BOUND('',#6180,.T.);
#6942=FACE_BOUND('',#6181,.T.);
#6943=FACE_BOUND('',#6182,.T.);
#6944=FACE_BOUND('',#6183,.T.);
#6945=FACE_BOUND('',#6184,.T.);
#6946=FACE_BOUND('',#6185,.T.);
#6947=FACE_BOUND('',#6186,.T.);
#6948=FACE_BOUND('',#6187,.T.);
#6949=FACE_BOUND('',#6188,.T.);
#6950=FACE_BOUND('',#6189,.T.);
#6951=FACE_BOUND('',#6190,.T.);
#6952=FACE_BOUND('',#6191,.T.);
#6953=FACE_BOUND('',#6192,.T.);
#6954=FACE_BOUND('',#6193,.T.);
#6955=FACE_BOUND('',#6194,.T.);
#6956=FACE_BOUND('',#6195,.T.);
#6957=FACE_BOUND('',#6196,.T.);
#6958=FACE_BOUND('',#6197,.T.);
#6959=FACE_BOUND('',#6198,.T.);
#7506=CYLINDRICAL_SURFACE('',#8578,0.0075);
#7507=CYLINDRICAL_SURFACE('',#8589,0.0085);
#7508=CYLINDRICAL_SURFACE('',#8595,0.008);
#7509=CYLINDRICAL_SURFACE('',#8602,0.009);
#7510=CYLINDRICAL_SURFACE('',#8612,0.0085);
#7854=ADVANCED_FACE('',(#6928,#6929),#7506,.F.);
#7855=ADVANCED_FACE('',(#6930,#6931),#1036,.F.);
#7856=ADVANCED_FACE('',(#6932,#6933),#1037,.F.);
#7857=ADVANCED_FACE('',(#6934,#6935),#44,.T.);
#7858=ADVANCED_FACE('',(#6936,#6937),#45,.T.);
#7859=ADVANCED_FACE('',(#6938,#6939),#7507,.T.);
#7860=ADVANCED_FACE('',(#6940,#6941),#46,.T.);
#7861=ADVANCED_FACE('',(#6942,#6943),#1038,.F.);
#7862=ADVANCED_FACE('',(#6944,#6945),#7508,.T.);
#7863=ADVANCED_FACE('',(#6946,#6947),#47,.F.);
#7864=ADVANCED_FACE('',(#6948),#48,.F.);
#7865=ADVANCED_FACE('',(#6949),#49,.F.);
#7866=ADVANCED_FACE('',(#6950,#6951),#7509,.T.);
#7867=ADVANCED_FACE('',(#6952,#6953),#24,.T.);
#7868=ADVANCED_FACE('',(#6954),#50,.T.);
#7869=ADVANCED_FACE('',(#6955),#51,.T.);
#7870=ADVANCED_FACE('',(#6956),#52,.T.);
#7871=ADVANCED_FACE('',(#6957),#53,.T.);
#7872=ADVANCED_FACE('',(#6958,#6959),#7510,.T.);
#8170=CLOSED_SHELL('',(#7854,#7855,#7856,#7857,#7858,#7859,#7860,#7861,
#7862,#7863,#7864,#7865,#7866,#7867,#7868,#7869,#7870,#7871,#7872));
#8176=STYLED_ITEM('',(#8182),#8221);
#8182=PRESENTATION_STYLE_ASSIGNMENT((#8188));
#8188=SURFACE_STYLE_USAGE(.BOTH.,#8194);
#8194=SURFACE_SIDE_STYLE('',(#8200));
#8200=SURFACE_STYLE_FILL_AREA(#8206);
#8206=FILL_AREA_STYLE('',(#8212));
#8212=FILL_AREA_STYLE_COLOUR('',#8216);
#8216=COLOUR_RGB('', 0.66274510, 0.83137255, 0.94901961);
#8221=MANIFOLD_SOLID_BREP('endcap__ DE    14671',#8170);
#8228=SHAPE_DEFINITION_REPRESENTATION(#18832,#8235);
#8235=SHAPE_REPRESENTATION('endcap__ DE    14671',(#8239),#18813);
#8239=AXIS2_PLACEMENT_3D('',#11098,#9192,#9193);
#8578=AXIS2_PLACEMENT_3D('',#13155,#9870,#9871);
#8579=AXIS2_PLACEMENT_3D('',#13156,#9872,#9873);
#8580=AXIS2_PLACEMENT_3D('',#13158,#9874,#9875);
#8581=AXIS2_PLACEMENT_3D('',#13160,#9876,#9877);
#8582=AXIS2_PLACEMENT_3D('',#13161,#9878,#9879);
#8583=AXIS2_PLACEMENT_3D('',#13163,#9880,#9881);
#8584=AXIS2_PLACEMENT_3D('',#13164,#9882,#9883);
#8585=AXIS2_PLACEMENT_3D('',#13166,#9884,#9885);
#8586=AXIS2_PLACEMENT_3D('',#13167,#9886,#9887);
#8587=AXIS2_PLACEMENT_3D('',#13181,#9888,#9889);
#8588=AXIS2_PLACEMENT_3D('',#13182,#9890,#9891);
#8589=AXIS2_PLACEMENT_3D('',#13184,#9892,#9893);
#8590=AXIS2_PLACEMENT_3D('',#13198,#9894,#9895);
#8591=AXIS2_PLACEMENT_3D('',#13199,#9896,#9897);
#8592=AXIS2_PLACEMENT_3D('',#13209,#9898,#9899);
#8593=AXIS2_PLACEMENT_3D('',#13210,#9900,#9901);
#8594=AXIS2_PLACEMENT_3D('',#13211,#9902,#9903);
#8595=AXIS2_PLACEMENT_3D('',#13213,#9904,#9905);
#8596=AXIS2_PLACEMENT_3D('',#13223,#9906,#9907);
#8597=AXIS2_PLACEMENT_3D('',#13224,#9908,#9909);
#8598=AXIS2_PLACEMENT_3D('',#13225,#9910,#9911);
#8599=AXIS2_PLACEMENT_3D('',#13239,#9912,#9913);
#8600=AXIS2_PLACEMENT_3D('',#13257,#9914,#9915);
#8601=AXIS2_PLACEMENT_3D('',#13258,#9916,#9917);
#8602=AXIS2_PLACEMENT_3D('',#13259,#9918,#9919);
#8603=AXIS2_PLACEMENT_3D('',#13273,#9920,#9921);
#8604=AXIS2_PLACEMENT_3D('',#13274,#9922,#9923);
#8605=AXIS2_PLACEMENT_3D('',#13275,#9924,#9925);
#8606=AXIS2_PLACEMENT_3D('',#13289,#9926,#9927);
#8607=AXIS2_PLACEMENT_3D('',#13295,#9928,#9929);
#8608=AXIS2_PLACEMENT_3D('',#13301,#9930,#9931);
#8609=AXIS2_PLACEMENT_3D('',#13313,#9932,#9933);
#8610=AXIS2_PLACEMENT_3D('',#13335,#9934,#9935);
#8611=AXIS2_PLACEMENT_3D('',#13336,#9936,#9937);
#8612=AXIS2_PLACEMENT_3D('',#13337,#9938,#9939);
#9192=DIRECTION('',(0.,0.,1.));
#9193=DIRECTION('',(1.,0.,0.));
#9870=DIRECTION('',(1.,0.,0.));
#9871=DIRECTION('',(0.,0.,-1.));
#9872=DIRECTION('',(1.,0.,0.));
#9873=DIRECTION('',(0.,0.,-1.));
#9874=DIRECTION('',(1.,0.,0.));
#9875=DIRECTION('',(0.,0.,-1.));
#9876=DIRECTION('',(-1.,-3.26422297091706E-17,-2.83054210170864E-17));
#9877=DIRECTION('',(3.26422297091706E-17,-1.,0.));
#9878=DIRECTION('',(1.,-1.52525712114884E-12,-4.12654899649895E-17));
#9879=DIRECTION('',(1.52525712114884E-12,1.,0.));
#9880=DIRECTION('',(1.,-2.37398034248512E-17,2.05857607396994E-17));
#9881=DIRECTION('',(2.37398034248512E-17,1.,0.));
#9882=DIRECTION('',(1.,1.1095485520975E-12,1.46545401316625E-17));
#9883=DIRECTION('',(-1.1095485520975E-12,1.,0.));
#9884=DIRECTION('',(1.,-1.52525712114884E-12,-4.12654899649895E-17));
#9885=DIRECTION('',(1.52525712114884E-12,1.,0.));
#9886=DIRECTION('',(1.,1.52523423639394E-12,4.77734628794545E-17));
#9887=DIRECTION('',(-1.52523423639394E-12,1.,0.));
#9888=DIRECTION('',(1.,1.1095485520975E-12,1.46545401316625E-17));
#9889=DIRECTION('',(-1.1095485520975E-12,1.,0.));
#9890=DIRECTION('',(1.,-1.10961798270237E-12,9.1670607747233E-18));
#9891=DIRECTION('',(1.10961798270237E-12,1.,0.));
#9892=DIRECTION('',(-1.,0.,-1.0449157878825E-16));
#9893=DIRECTION('',(-1.0449157878825E-16,0.,1.));
#9894=DIRECTION('',(-1.,0.,-1.0449157878825E-16));
#9895=DIRECTION('',(-1.0449157878825E-16,0.,1.));
#9896=DIRECTION('',(1.,1.5253472309144E-12,1.6070040430106E-17));
#9897=DIRECTION('',(-1.5253472309144E-12,1.,0.));
#9898=DIRECTION('',(1.,-1.52537011566931E-12,-9.71439789292615E-18));
#9899=DIRECTION('',(1.52537011566931E-12,1.,0.));
#9900=DIRECTION('',(-1.,9.57477243706982E-18,9.40580586465046E-18));
#9901=DIRECTION('',(-9.57477243706982E-18,-1.,0.));
#9902=DIRECTION('',(1.,-1.28458696201097E-12,-2.92084213202575E-17));
#9903=DIRECTION('',(1.28458696201097E-12,1.,0.));
#9904=DIRECTION('',(-1.,0.,-1.11022302462516E-16));
#9905=DIRECTION('',(-1.11022302462516E-16,0.,1.));
#9906=DIRECTION('',(-1.,0.,-1.11022302462516E-16));
#9907=DIRECTION('',(-1.11022302462516E-16,0.,1.));
#9908=DIRECTION('',(1.,-1.28458696201097E-12,-2.92084213202575E-17));
#9909=DIRECTION('',(1.28458696201097E-12,1.,0.));
#9910=DIRECTION('',(-1.,0.,0.));
#9911=DIRECTION('',(0.,0.,1.));
#9912=DIRECTION('',(1.,-1.06677650229913E-10,1.79070058553459E-17));
#9913=DIRECTION('',(1.06677650229913E-10,1.,0.));
#9914=DIRECTION('',(1.,1.06677627345158E-10,-7.52576163854158E-18));
#9915=DIRECTION('',(-1.06677627345158E-10,1.,0.));
#9916=DIRECTION('',(-1.,0.,-1.04189432305107E-15));
#9917=DIRECTION('',(-1.04189432305107E-15,0.,1.));
#9918=DIRECTION('',(-1.,0.,0.));
#9919=DIRECTION('',(0.,0.,1.));
#9920=DIRECTION('',(-1.,0.,0.));
#9921=DIRECTION('',(0.,0.,1.));
#9922=DIRECTION('',(-1.,0.,-1.04189432305107E-15));
#9923=DIRECTION('',(-1.04189432305107E-15,0.,1.));
#9924=DIRECTION('',(-1.,0.,-1.04189432305107E-15));
#9925=DIRECTION('',(-1.04189432305107E-15,0.,1.));
#9926=DIRECTION('',(1.,3.57212507207529E-11,7.69107850575555E-18));
#9927=DIRECTION('',(-3.57212507207529E-11,1.,0.));
#9928=DIRECTION('',(1.,3.57212507207529E-11,7.69107850575555E-18));
#9929=DIRECTION('',(-3.57212507207529E-11,1.,0.));
#9930=DIRECTION('',(1.,-3.57214956501127E-11,-1.55638472566498E-17));
#9931=DIRECTION('',(3.57214956501127E-11,1.,0.));
#9932=DIRECTION('',(1.,1.13344866900787E-10,1.0907594486052E-16));
#9933=DIRECTION('',(-1.13344866900787E-10,1.,0.));
#9934=DIRECTION('',(1.,-1.13344929948816E-10,-1.04122921954656E-16));
#9935=DIRECTION('',(1.13344929948816E-10,1.,0.));
#9936=DIRECTION('',(1.,-1.13344929948816E-10,-1.04122921954656E-16));
#9937=DIRECTION('',(1.13344929948816E-10,1.,0.));
#9938=DIRECTION('',(-1.,0.,2.61228946970625E-17));
#9939=DIRECTION('',(2.61228946970625E-17,0.,1.));
#11098=CARTESIAN_POINT('',(0.,0.,0.));
#13155=CARTESIAN_POINT('',(-0.00525,0.,0.));
#13156=CARTESIAN_POINT('',(0.00525,0.,0.));
#13157=CARTESIAN_POINT('',(0.00525,0.,-0.0075));
#13158=CARTESIAN_POINT('',(-0.00525,0.,0.));
#13159=CARTESIAN_POINT('',(-0.00525,0.,-0.0075));
#13160=CARTESIAN_POINT('',(0.00525,-4.9439619065339E-19,-2.41993924898764E-18));
#13161=CARTESIAN_POINT('',(0.00525000000022048,1.9259841093292E-13,4.25226277214903E-19));
#13162=CARTESIAN_POINT('',(0.00525000000023268,0.00800000000074963,4.25226277214903E-19));
#13163=CARTESIAN_POINT('',(-0.00525,-2.64545330086463E-19,6.93889390390723E-19));
#13164=CARTESIAN_POINT('',(-0.00525000000022048,1.92806907086136E-13,-4.70350263194859E-19));
#13165=CARTESIAN_POINT('',(-0.00525000000023268,0.0110000000007498,-4.70350263194859E-19));
#13166=CARTESIAN_POINT('',(0.00474999999987469,1.93361039494021E-13,4.45859022211667E-19));
#13167=CARTESIAN_POINT('',(0.00475000000055703,-1.93360444885966E-13,-1.48019874151438E-19));
#13168=CARTESIAN_POINT('',(0.00474999987540352,-1.74337662513279E-12,-0.00850000000012328));
#13169=CARTESIAN_POINT('',(0.00474999987527852,-4.86361310422452E-12,0.00850000000012328));
#13170=CARTESIAN_POINT('',(0.00475000000055704,-4.86361227985766E-12,0.00850000000024656));
#13171=CARTESIAN_POINT('',(0.00475000000055534,-0.00111264740275087,0.0084999999995846));
#13172=CARTESIAN_POINT('',(0.00475000000055195,-0.00333742350645399,0.00805742090693034));
#13173=CARTESIAN_POINT('',(0.00475000000054763,-0.00616690169649648,0.00616688297620523));
#13174=CARTESIAN_POINT('',(0.00475000000054475,-0.00805741556199689,0.00333749301577175));
#13175=CARTESIAN_POINT('',(0.00475000000054374,-0.00872129221938764,-1.60072261902693E-12));
#13176=CARTESIAN_POINT('',(0.00475000000054475,-0.00805741556077174,-0.00333749301872954));
#13177=CARTESIAN_POINT('',(0.00475000000054763,-0.00616690169423269,-0.00616688297846902));
#13178=CARTESIAN_POINT('',(0.00475000000055195,-0.00333742350349621,-0.00805742090815546));
#13179=CARTESIAN_POINT('',(0.00475000000055534,-0.00111264739963064,-0.00849999999999304));
#13180=CARTESIAN_POINT('',(0.00475000000055704,-1.7433859526852E-12,-0.00850000000024656));
#13181=CARTESIAN_POINT('',(-0.00474999999987469,1.93361681362568E-13,-4.6302299312396E-19));
#13182=CARTESIAN_POINT('',(-0.00424999999977952,1.92803729271711E-13,2.29417486392181E-19));
#13183=CARTESIAN_POINT('',(-0.00424999999976731,0.0110000000007498,2.29417486392181E-19));
#13184=CARTESIAN_POINT('',(-0.007263258046,0.,2.86039083864497E-51));
#13185=CARTESIAN_POINT('',(0.00425,-5.61175846058392E-12,-0.0085));
#13186=CARTESIAN_POINT('',(0.00425,-0.00111264740337218,-0.00849999999926542));
#13187=CARTESIAN_POINT('',(0.00425,-0.00333742350679297,-0.00805742090655498));
#13188=CARTESIAN_POINT('',(0.00425,-0.00616690169647487,-0.00616688297600855));
#13189=CARTESIAN_POINT('',(0.00425,-0.008057415561805,-0.00333749301594122));
#13190=CARTESIAN_POINT('',(0.00425,-0.00872129221928992,1.00565516758058E-12));
#13191=CARTESIAN_POINT('',(0.00425,-0.00805741556103531,0.00333749301779943));
#13192=CARTESIAN_POINT('',(0.00425,-0.00616690169505265,0.00616688297743077));
#13193=CARTESIAN_POINT('',(0.00425,-0.00333742350493477,0.00805742090732466));
#13194=CARTESIAN_POINT('',(0.00425,-0.0011126474014119,0.00849999999952203));
#13195=CARTESIAN_POINT('',(0.00425,-3.65148430959518E-12,0.0085));
#13196=CARTESIAN_POINT('',(0.00425,-2.88824233062088E-12,0.0085));
#13197=CARTESIAN_POINT('',(0.00425000037472148,-1.74337673725018E-12,-0.00850000000012328));
#13198=CARTESIAN_POINT('',(0.00425,0.,1.20303851022306E-18));
#13199=CARTESIAN_POINT('',(0.00425000000012531,1.93360815258866E-13,-2.80147189803738E-19));
#13200=CARTESIAN_POINT('',(0.00374999999977953,-2.71834574313571E-12,0.00800000000055703));
#13201=CARTESIAN_POINT('',(0.00374999999978272,-0.00209439510486201,0.00799999999979495));
#13202=CARTESIAN_POINT('',(0.00374999999978908,-0.00626651094914304,0.00626889299797267));
#13203=CARTESIAN_POINT('',(0.00374999999979305,-0.00886674452618622,-5.97131919231566E-13));
#13204=CARTESIAN_POINT('',(0.00374999999978908,-0.00626651094829869,-0.00626889299881671));
#13205=CARTESIAN_POINT('',(0.00374999999978272,-0.00209439510378449,-0.00800000000007704));
#13206=CARTESIAN_POINT('',(0.00374999999977953,-1.64082385457008E-12,-0.00800000000055703));
#13207=CARTESIAN_POINT('',(0.00374999987488976,-2.71834529339123E-12,0.00800000000027852));
#13208=CARTESIAN_POINT('',(0.00374999987488976,-1.64082717271973E-12,-0.00800000000040351));
#13209=CARTESIAN_POINT('',(0.00374999999977952,-1.92598860655761E-13,1.48862633905608E-19));
#13210=CARTESIAN_POINT('',(-0.00425,-2.64545330086463E-19,-6.93889390390723E-19));
#13211=CARTESIAN_POINT('',(-0.00425000000022048,1.94006876112138E-13,-2.13954723767001E-19));
#13212=CARTESIAN_POINT('',(-0.00425000000020828,0.00949999999963698,-2.13954723767001E-19));
#13213=CARTESIAN_POINT('',(-0.007263258046,0.,2.83936039877452E-51));
#13214=CARTESIAN_POINT('',(0.001457106781,-5.28165502172604E-12,-0.008));
#13215=CARTESIAN_POINT('',(0.001457106781,-0.00209439510694832,-0.00799999999861726));
#13216=CARTESIAN_POINT('',(0.001457106781,-0.00626651094977711,-0.00626889299625425));
#13217=CARTESIAN_POINT('',(0.001457106781,-0.00886674452547288,1.0224280356647E-12));
#13218=CARTESIAN_POINT('',(0.001457106781,-0.00626651094833137,0.00626889299769943));
#13219=CARTESIAN_POINT('',(0.001457106781,-0.00209439510510336,0.00799999999910028));
#13220=CARTESIAN_POINT('',(0.001457106781,-3.43669111491311E-12,0.008));
#13221=CARTESIAN_POINT('',(0.001457106781,-2.7183457229373E-12,0.008));
#13222=CARTESIAN_POINT('',(0.001457107156,-2.28165122079125E-12,-0.008));
#13223=CARTESIAN_POINT('',(0.001457106781,0.,9.68154981406677E-19));
#13224=CARTESIAN_POINT('',(-0.00374999999987468,1.93364582630688E-13,-2.28558934437229E-19));
#13225=CARTESIAN_POINT('',(-0.00375,0.,0.));
#13226=CARTESIAN_POINT('',(-0.00374999987527851,-1.8459280570297E-12,-0.00899999999987672));
#13227=CARTESIAN_POINT('',(-0.00374999987527851,-1.22168301791654E-12,0.00899999999987672));
#13228=CARTESIAN_POINT('',(-0.00375000000055703,-1.22168309480298E-12,0.00899999999975343));
#13229=CARTESIAN_POINT('',(-0.00375000000055552,-0.00117809724617388,0.00899999999961883));
#13230=CARTESIAN_POINT('',(-0.00375000000055249,-0.00353374253293338,0.00853138684369092));
#13231=CARTESIAN_POINT('',(-0.00375000000054865,-0.0065296606176239,0.00652964080030454));
#13232=CARTESIAN_POINT('',(-0.00375000000054607,-0.00853138118227796,0.00353381613659912));
#13233=CARTESIAN_POINT('',(-0.00375000000054517,-0.00923430940871994,3.20239732450106E-13));
#13234=CARTESIAN_POINT('',(-0.00375000000054607,-0.00853138118252307,-0.00353381613600736));
#13235=CARTESIAN_POINT('',(-0.00375000000054865,-0.0065296606180768,-0.00652964079985164));
#13236=CARTESIAN_POINT('',(-0.00375000000055249,-0.00353374253352514,-0.00853138684344582));
#13237=CARTESIAN_POINT('',(-0.00375000000055552,-0.00117809724679812,-0.00899999999953711));
#13238=CARTESIAN_POINT('',(-0.00375000000055703,-1.845925958314E-12,-0.00899999999975343));
#13239=CARTESIAN_POINT('',(0.0014571067816285,-5.47396505703968E-13,6.65202876568241E-20));
#13240=CARTESIAN_POINT('',(0.00110355339071671,1.58556738773517E-17,0.00814644660952611));
#13241=CARTESIAN_POINT('',(0.00119611345182742,2.63259265651322E-16,0.00805388654805348));
#13242=CARTESIAN_POINT('',(0.00132620708739174,-1.64577341757993E-15,0.00799999999964119));
#13243=CARTESIAN_POINT('',(0.0014571067814045,1.67659206997871E-17,0.00799999999958255));
#13244=CARTESIAN_POINT('',(0.00110355330247001,-2.9115133713822E-12,0.0081464466976514));
#13245=CARTESIAN_POINT('',(0.00110355339071671,-1.6708634304086E-12,-0.00814644660952611));
#13246=CARTESIAN_POINT('',(0.00110355339048919,-0.00213273473648634,-0.00814644660922211));
#13247=CARTESIAN_POINT('',(0.00110355339003597,-0.0063812246085619,-0.0063836502643864));
#13248=CARTESIAN_POINT('',(0.00110355338975351,-0.00902905761052969,-6.87539018106074E-13));
#13249=CARTESIAN_POINT('',(0.00110355339003597,-0.00638122460953407,0.00638365026341459));
#13250=CARTESIAN_POINT('',(0.00110355339048919,-0.00213273473772698,0.00814644660889731));
#13251=CARTESIAN_POINT('',(0.00110355339071671,-2.91151058367133E-12,0.00814644660952611));
#13252=CARTESIAN_POINT('',(0.00110355330262237,-1.67086175802321E-12,-0.00814644669762802));
#13253=CARTESIAN_POINT('',(0.0014571067814045,-3.13787920007409E-17,-0.00799999999958255));
#13254=CARTESIAN_POINT('',(0.00132620708739174,-1.66845701558407E-15,-0.00799999999964119));
#13255=CARTESIAN_POINT('',(0.00119611345182742,2.65760905900004E-16,-0.00805388654805348));
#13256=CARTESIAN_POINT('',(0.00110355339071671,4.46112367465754E-17,-0.00814644660952611));
#13257=CARTESIAN_POINT('',(0.0014571067816285,5.47397208070073E-13,-5.45798719985721E-19));
#13258=CARTESIAN_POINT('',(0.00110355339112794,0.,-1.04204690494148E-15));
#13259=CARTESIAN_POINT('',(-0.007263258046,0.,0.));
#13260=CARTESIAN_POINT('',(-0.003116025404,-3.86627750427725E-12,0.009));
#13261=CARTESIAN_POINT('',(-0.003116025404,-0.00117809724855378,0.0089999999994939));
#13262=CARTESIAN_POINT('',(-0.003116025404,-0.00353374253463681,0.00853138684304964));
#13263=CARTESIAN_POINT('',(-0.003116025404,-0.00652966061829104,0.00652964079963258));
#13264=CARTESIAN_POINT('',(-0.003116025404,-0.00853138118227268,0.00353381613649351));
#13265=CARTESIAN_POINT('',(-0.003116025404,-0.00923430940865992,1.06481072844012E-12));
#13266=CARTESIAN_POINT('',(-0.003116025404,-0.00853138118308765,-0.003533816134526));
#13267=CARTESIAN_POINT('',(-0.003116025404,-0.00652966061979692,-0.0065296407981267));
#13268=CARTESIAN_POINT('',(-0.003116025404,-0.00353374253660432,-0.00853138684223469));
#13269=CARTESIAN_POINT('',(-0.003116025404,-0.00117809725062936,-0.00899999999922221));
#13270=CARTESIAN_POINT('',(-0.003116025404,-5.9418618994418E-12,-0.009));
#13271=CARTESIAN_POINT('',(-0.00311602552873704,-1.84592937600593E-12,-0.00899999999997601));
#13272=CARTESIAN_POINT('',(-0.00311602552873704,1.12499936185184E-12,0.00899999999997601));
#13273=CARTESIAN_POINT('',(-0.003116025404,0.,0.));
#13274=CARTESIAN_POINT('',(0.00925000000025689,0.,-1.03355916846639E-15));
#13275=CARTESIAN_POINT('',(0.000896446609127943,0.,-1.04226268832191E-15));
#13276=CARTESIAN_POINT('',(0.000896446947516299,-2.38248677279272E-12,-0.00835355305274167));
#13277=CARTESIAN_POINT('',(0.000896446609127934,-2.83848445413882E-12,0.00835355339112793));
#13278=CARTESIAN_POINT('',(0.000896446609127957,-5.51507340218912E-12,-0.00835355339113002));
#13279=CARTESIAN_POINT('',(0.000896446609127957,-0.00109347758700829,-0.0083535533904081));
#13280=CARTESIAN_POINT('',(0.000896446609127956,-0.00327992299444752,-0.00791859949855468));
#13281=CARTESIAN_POINT('',(0.000896446609127955,-0.00606065206815843,-0.00606063367022831));
#13282=CARTESIAN_POINT('',(0.000896446609127951,-0.00791859424588842,-0.00327999130602281));
#13283=CARTESIAN_POINT('',(0.000896446609127948,-0.00857103296393836,9.87285581686735E-13));
#13284=CARTESIAN_POINT('',(0.000896446609127945,-0.00791859424513199,0.00327999130784692));
#13285=CARTESIAN_POINT('',(0.000896446609127942,-0.00606065206676072,0.00606063367162394));
#13286=CARTESIAN_POINT('',(0.00089644660912794,-0.00327992299262134,0.00791859949930901));
#13287=CARTESIAN_POINT('',(0.000896446609127939,-0.00109347758508179,0.00835355339065819));
#13288=CARTESIAN_POINT('',(0.000896446609127939,-3.58857283965566E-12,0.00835355339112793));
#13289=CARTESIAN_POINT('',(-0.00311602540366083,1.89369138590977E-13,4.60164670987285E-19));
#13290=CARTESIAN_POINT('',(-0.00311602540347409,-2.08135904343245E-17,0.00899999999995202));
#13291=CARTESIAN_POINT('',(-0.00276695955312565,-2.17671273402248E-15,0.00899999999988684));
#13292=CARTESIAN_POINT('',(-0.00242453292500672,-2.5821733949979E-16,0.00880229989405671));
#13293=CARTESIAN_POINT('',(-0.00224999999965417,-1.04806440198648E-18,0.0085000000001643));
#13294=CARTESIAN_POINT('',(-0.00224999987482708,-1.83738466424475E-19,0.00850000000008215));
#13295=CARTESIAN_POINT('',(-0.00224999999965417,2.2030464917804E-13,4.66825340357479E-19));
#13296=CARTESIAN_POINT('',(-0.00224999987482708,-1.74337942337899E-12,-0.00850000000008215));
#13297=CARTESIAN_POINT('',(-0.00224999999965417,-1.44542388119606E-17,-0.0085000000001643));
#13298=CARTESIAN_POINT('',(-0.00242453292500672,-2.56372140876474E-16,-0.00880229989405671));
#13299=CARTESIAN_POINT('',(-0.00276695955312565,-2.15760081618848E-15,-0.00899999999988684));
#13300=CARTESIAN_POINT('',(-0.00311602540347409,1.49516727692217E-17,-0.00899999999995202));
#13301=CARTESIAN_POINT('',(-0.00311602540366083,-1.89369495587902E-13,-4.56753702428283E-19));
#13302=CARTESIAN_POINT('',(-0.00224999999965417,-1.74337645012797E-12,-0.0085000000001643));
#13303=CARTESIAN_POINT('',(-0.00224999999969392,-0.00111264739985699,-0.00849999999996493));
#13304=CARTESIAN_POINT('',(-0.00224999999977339,-0.00333742350419627,-0.00805742090804886));
#13305=CARTESIAN_POINT('',(-0.00224999999987446,-0.00616690169538636,-0.00616688297774479));
#13306=CARTESIAN_POINT('',(-0.002249999999942,-0.00805741556187121,-0.00333749301710294));
#13307=CARTESIAN_POINT('',(-0.00224999999996571,-0.00872129221981244,8.94381676439934E-13));
#13308=CARTESIAN_POINT('',(-0.002249999999942,-0.00805741556118667,0.00333749301875555));
#13309=CARTESIAN_POINT('',(-0.00224999999987446,-0.00616690169412152,0.00616688297900963));
#13310=CARTESIAN_POINT('',(-0.00224999999977339,-0.00333742350254365,0.00805742090873338));
#13311=CARTESIAN_POINT('',(-0.00224999999969392,-0.00111264739811362,0.00850000000019314));
#13312=CARTESIAN_POINT('',(-0.00224999999965417,-1.35791309261817E-17,0.0085000000001643));
#13313=CARTESIAN_POINT('',(0.000542893218371495,5.47403523416524E-13,1.10783975326665E-19));
#13314=CARTESIAN_POINT('',(0.000896446609283292,-1.46288588890009E-17,0.0083535533904739));
#13315=CARTESIAN_POINT('',(0.000803886548172581,-5.03456191566966E-16,0.00844611345194653));
#13316=CARTESIAN_POINT('',(0.00067379291260826,-1.94773245151004E-15,0.00850000000035882));
#13317=CARTESIAN_POINT('',(0.000542893218595496,1.69082711704543E-17,0.00850000000041746));
#13318=CARTESIAN_POINT('',(0.000542893093797748,-2.12500021499821E-12,0.00850000000020873));
#13319=CARTESIAN_POINT('',(0.000542893218595496,-2.12499836668962E-12,0.00850000000041746));
#13320=CARTESIAN_POINT('',(0.000542893218721609,-0.00111264740011923,0.00850000000006764));
#13321=CARTESIAN_POINT('',(0.000542893218973776,-0.00333742350416026,0.00805742090796045));
#13322=CARTESIAN_POINT('',(0.000542893219294483,-0.00616690169492879,0.00616688297771508));
#13323=CARTESIAN_POINT('',(0.000542893219508763,-0.00805741556119902,0.00333749301739052));
#13324=CARTESIAN_POINT('',(0.00054289321958401,-0.00872129221924304,-1.95784323807277E-13));
#13325=CARTESIAN_POINT('',(0.000542893219508763,-0.00805741556104918,-0.00333749301775226));
#13326=CARTESIAN_POINT('',(0.000542893219294483,-0.00616690169465192,-0.00616688297799194));
#13327=CARTESIAN_POINT('',(0.000542893218973777,-0.00333742350379851,-0.00805742090811029));
#13328=CARTESIAN_POINT('',(0.000542893218721609,-0.00111264739973761,-0.0085000000001176));
#13329=CARTESIAN_POINT('',(0.000542893218595496,-1.74337804822321E-12,-0.00850000000041746));
#13330=CARTESIAN_POINT('',(0.000542893093922748,-1.7433764476282E-12,-0.00850000000020873));
#13331=CARTESIAN_POINT('',(0.000542893218595496,1.61471761803093E-18,-0.00850000000041746));
#13332=CARTESIAN_POINT('',(0.000673792912608261,-1.96176775230103E-15,-0.00850000000035882));
#13333=CARTESIAN_POINT('',(0.000803886548172583,-5.16138536658815E-16,-0.00844611345194653));
#13334=CARTESIAN_POINT('',(0.000896446609283294,-2.59491966845735E-17,-0.0083535533904739));
#13335=CARTESIAN_POINT('',(0.000542893218371494,-5.47404119942789E-13,5.87721542220263E-20));
#13336=CARTESIAN_POINT('',(0.000542893218595497,-5.47404119968178E-13,5.87721541987024E-20));
#13337=CARTESIAN_POINT('',(-0.007263258046,0.,2.44324620272917E-53));
#18809=MECHANICAL_DESIGN_GEOMETRIC_PRESENTATION_REPRESENTATION('',(#8176),#18810);
#18810=(
GEOMETRIC_REPRESENTATION_CONTEXT(3)
GLOBAL_UNCERTAINTY_ASSIGNED_CONTEXT((#18817))
GLOBAL_UNIT_ASSIGNED_CONTEXT((#18826,#18825,#18824))
REPRESENTATION_CONTEXT('MAS-697','TOP_LEVEL_ASSEMBLY_PART')
);
#18813=(
GEOMETRIC_REPRESENTATION_CONTEXT(3)
GLOBAL_UNCERTAINTY_ASSIGNED_CONTEXT((#18820))
GLOBAL_UNIT_ASSIGNED_CONTEXT((#18826,#18825,#18824))
REPRESENTATION_CONTEXT('endcap__ DE    14671','COMPONENT_PART')
);
#18817=UNCERTAINTY_MEASURE_WITH_UNIT(LENGTH_MEASURE(1.E-8),#18826,
'DISTANCE_ACCURACY_VALUE','Maximum Tolerance applied to model');
#18820=UNCERTAINTY_MEASURE_WITH_UNIT(LENGTH_MEASURE(2.E-5),#18826,
'DISTANCE_ACCURACY_VALUE','Maximum Tolerance applied to model');
#18824=(
NAMED_UNIT(*)
SI_UNIT($,.STERADIAN.)
SOLID_ANGLE_UNIT()
);
#18825=(
NAMED_UNIT(*)
PLANE_ANGLE_UNIT()
SI_UNIT($,.RADIAN.)
);
#18826=(
LENGTH_UNIT()
NAMED_UNIT(*)
SI_UNIT($,.METRE.)
);
#18832=PRODUCT_DEFINITION_SHAPE('','',#18843);
#18843=PRODUCT_DEFINITION('','',#18857,#18850);
#18850=PRODUCT_DEFINITION_CONTEXT('',#18890,'design');
#18857=PRODUCT_DEFINITION_FORMATION_WITH_SPECIFIED_SOURCE('','',#18871,
 .NOT_KNOWN.);
#18871=PRODUCT('endcap__ DE    14671','endcap__ DE    14671',
'endcap__ DE    14671',(#18885));
#18885=PRODUCT_CONTEXT('',#18890,'mechanical');
#18890=APPLICATION_CONTEXT('managed model based 3d engineering');
ENDSEC;
END-ISO-10303-21;
